ISO-10303-21;
HEADER;
/* Generated by software containing ST-Developer
 * from STEP Tools, Inc. (www.steptools.com) 
 */

FILE_DESCRIPTION(
/* description */ ('STEP AP214'),
/* implementation_level */ '2;1');

FILE_NAME(
/* name */ 'Small Pin.step',
/* time_stamp */ '2026-10-06T11:11:25-07:00',
/* author */ (''),
/* organization */ (''),
/* preprocessor_version */ 'ST-DEVELOPER v20.2',
/* originating_system */ 'Autodesk Translation Framework v15.15.0.0',
/* authorisation */ '');

FILE_SCHEMA (('AUTOMOTIVE_DESIGN { 1 0 10303 214 3 1 1 }'));
ENDSEC;

DATA;
#10=MECHANICAL_DESIGN_GEOMETRIC_PRESENTATION_REPRESENTATION('',(#706),#47717);
#682=SHAPE_REPRESENTATION_RELATIONSHIP('SRR','None',#47769,#694);
#694=ADVANCED_BREP_SHAPE_REPRESENTATION('',(#718),#47713);
#706=STYLED_ITEM('',(#47830),#718);
#718=MANIFOLD_SOLID_BREP('Body1',#8933);
#749=FACE_BOUND('',#3051,.T.);
#750=FACE_BOUND('',#3053,.T.);
#869=PLANE('',#9822);
#870=PLANE('',#9823);
#1329=LINE('',#45913,#1816);
#1816=VECTOR('',#11904,1.);
#2040=CYLINDRICAL_SURFACE('',#9819,1.);
#2508=FACE_OUTER_BOUND('',#3047,.T.);
#2509=FACE_OUTER_BOUND('',#3048,.T.);
#2510=FACE_OUTER_BOUND('',#3049,.T.);
#2511=FACE_OUTER_BOUND('',#3050,.T.);
#2512=FACE_OUTER_BOUND('',#3052,.T.);
#3047=EDGE_LOOP('',(#8101,#8102,#8103));
#3048=EDGE_LOOP('',(#8104,#8105,#8106));
#3049=EDGE_LOOP('',(#8107,#8108,#8109,#8110));
#3050=EDGE_LOOP('',(#8111));
#3051=EDGE_LOOP('',(#8112));
#3052=EDGE_LOOP('',(#8113));
#3053=EDGE_LOOP('',(#8114));
#3462=CIRCLE('',#9814,1.20000000000001);
#3463=CIRCLE('',#9815,1.19999999999999);
#3464=CIRCLE('',#9817,1.20000000000001);
#3465=CIRCLE('',#9818,1.19999999999999);
#3466=CIRCLE('',#9820,1.);
#3467=CIRCLE('',#9821,1.);
#4295=VERTEX_POINT('',#45900);
#4296=VERTEX_POINT('',#45902);
#4297=VERTEX_POINT('',#45905);
#4298=VERTEX_POINT('',#45907);
#4299=VERTEX_POINT('',#45910);
#4300=VERTEX_POINT('',#45912);
#5576=EDGE_CURVE('',#4295,#4295,#3462,.T.);
#5577=EDGE_CURVE('',#4295,#4296,#3463,.T.);
#5578=EDGE_CURVE('',#4297,#4297,#3464,.T.);
#5579=EDGE_CURVE('',#4298,#4297,#3465,.T.);
#5580=EDGE_CURVE('',#4299,#4299,#3466,.T.);
#5581=EDGE_CURVE('',#4299,#4300,#1329,.T.);
#5582=EDGE_CURVE('',#4300,#4300,#3467,.T.);
#8101=ORIENTED_EDGE('',*,*,#5576,.F.);
#8102=ORIENTED_EDGE('',*,*,#5577,.T.);
#8103=ORIENTED_EDGE('',*,*,#5577,.F.);
#8104=ORIENTED_EDGE('',*,*,#5578,.T.);
#8105=ORIENTED_EDGE('',*,*,#5579,.F.);
#8106=ORIENTED_EDGE('',*,*,#5579,.T.);
#8107=ORIENTED_EDGE('',*,*,#5580,.F.);
#8108=ORIENTED_EDGE('',*,*,#5581,.T.);
#8109=ORIENTED_EDGE('',*,*,#5582,.F.);
#8110=ORIENTED_EDGE('',*,*,#5581,.F.);
#8111=ORIENTED_EDGE('',*,*,#5578,.F.);
#8112=ORIENTED_EDGE('',*,*,#5582,.T.);
#8113=ORIENTED_EDGE('',*,*,#5576,.T.);
#8114=ORIENTED_EDGE('',*,*,#5580,.T.);
#8409=SPHERICAL_SURFACE('',#9813,1.2);
#8410=SPHERICAL_SURFACE('',#9816,1.2);
#8858=ADVANCED_FACE('',(#2508),#8409,.T.);
#8859=ADVANCED_FACE('',(#2509),#8410,.T.);
#8860=ADVANCED_FACE('',(#2510),#2040,.T.);
#8861=ADVANCED_FACE('',(#2511,#749),#869,.F.);
#8862=ADVANCED_FACE('',(#2512,#750),#870,.F.);
#8933=CLOSED_SHELL('',(#8858,#8859,#8860,#8861,#8862));
#9812=AXIS2_PLACEMENT_3D('',#45898,#11886,#11887);
#9813=AXIS2_PLACEMENT_3D('',#45899,#11888,#11889);
#9814=AXIS2_PLACEMENT_3D('',#45901,#11890,#11891);
#9815=AXIS2_PLACEMENT_3D('',#45903,#11892,#11893);
#9816=AXIS2_PLACEMENT_3D('',#45904,#11894,#11895);
#9817=AXIS2_PLACEMENT_3D('',#45906,#11896,#11897);
#9818=AXIS2_PLACEMENT_3D('',#45908,#11898,#11899);
#9819=AXIS2_PLACEMENT_3D('',#45909,#11900,#11901);
#9820=AXIS2_PLACEMENT_3D('',#45911,#11902,#11903);
#9821=AXIS2_PLACEMENT_3D('',#45914,#11905,#11906);
#9822=AXIS2_PLACEMENT_3D('',#45915,#11907,#11908);
#9823=AXIS2_PLACEMENT_3D('',#45916,#11909,#11910);
#11886=DIRECTION('axis',(0.,0.,1.));
#11887=DIRECTION('refdir',(1.,0.,0.));
#11888=DIRECTION('center_axis',(0.,0.,1.));
#11889=DIRECTION('ref_axis',(1.,0.,0.));
#11890=DIRECTION('center_axis',(0.,0.,1.));
#11891=DIRECTION('ref_axis',(1.,0.,0.));
#11892=DIRECTION('center_axis',(0.,-1.,0.));
#11893=DIRECTION('ref_axis',(-1.,0.,0.));
#11894=DIRECTION('center_axis',(0.,0.,1.));
#11895=DIRECTION('ref_axis',(1.,0.,0.));
#11896=DIRECTION('center_axis',(0.,0.,1.));
#11897=DIRECTION('ref_axis',(1.,0.,0.));
#11898=DIRECTION('center_axis',(0.,-1.,0.));
#11899=DIRECTION('ref_axis',(-1.,0.,0.));
#11900=DIRECTION('center_axis',(0.,0.,-1.));
#11901=DIRECTION('ref_axis',(-1.,0.,0.));
#11902=DIRECTION('center_axis',(0.,0.,-1.));
#11903=DIRECTION('ref_axis',(-1.,0.,0.));
#11904=DIRECTION('',(0.,0.,1.));
#11905=DIRECTION('center_axis',(0.,0.,1.));
#11906=DIRECTION('ref_axis',(1.,0.,0.));
#11907=DIRECTION('center_axis',(0.,0.,1.));
#11908=DIRECTION('ref_axis',(1.,0.,0.));
#11909=DIRECTION('center_axis',(0.,0.,-1.));
#11910=DIRECTION('ref_axis',(1.,0.,0.));
#45898=CARTESIAN_POINT('',(0.,0.,0.));
#45899=CARTESIAN_POINT('Origin',(-84.8548278771908,-59.0746191263193,171.485485069079));
#45900=CARTESIAN_POINT('',(-86.0548278771908,-59.0746191263193,171.485485069079));
#45901=CARTESIAN_POINT('Origin',(-84.8548278771908,-59.0746191263193,171.485485069079));
#45902=CARTESIAN_POINT('',(-84.8548278771908,-59.0746191263193,170.285485069079));
#45903=CARTESIAN_POINT('Origin',(-84.8548278771908,-59.0746191263193,171.485485069079));
#45904=CARTESIAN_POINT('Origin',(-84.8548278771908,-59.0746191263193,180.485485069079));
#45905=CARTESIAN_POINT('',(-86.0548278771908,-59.0746191263193,180.485485069079));
#45906=CARTESIAN_POINT('Origin',(-84.8548278771908,-59.0746191263193,180.485485069079));
#45907=CARTESIAN_POINT('',(-84.8548278771908,-59.0746191263193,181.685485069079));
#45908=CARTESIAN_POINT('Origin',(-84.8548278771908,-59.0746191263193,180.485485069079));
#45909=CARTESIAN_POINT('Origin',(-84.8548278771908,-59.0746191263193,180.485485069079));
#45910=CARTESIAN_POINT('',(-83.8548278771908,-59.0746191263193,171.485485069079));
#45911=CARTESIAN_POINT('Origin',(-84.8548278771908,-59.0746191263193,171.485485069079));
#45912=CARTESIAN_POINT('',(-83.8548278771908,-59.0746191263193,180.485485069079));
#45913=CARTESIAN_POINT('',(-83.8548278771908,-59.0746191263193,180.485485069079));
#45914=CARTESIAN_POINT('Origin',(-84.8548278771908,-59.0746191263193,180.485485069079));
#45915=CARTESIAN_POINT('Origin',(-84.8548278771908,-59.0746191263193,180.485485069079));
#45916=CARTESIAN_POINT('Origin',(-84.8548278771908,-59.0746191263193,171.485485069079));
#47699=UNCERTAINTY_MEASURE_WITH_UNIT(LENGTH_MEASURE(0.01),#47718,
'DISTANCE_ACCURACY_VALUE',
'Maximum model space distance between geometric entities at asserted c
onnectivities');
#47703=UNCERTAINTY_MEASURE_WITH_UNIT(LENGTH_MEASURE(0.01),#47718,
'DISTANCE_ACCURACY_VALUE',
'Maximum model space distance between geometric entities at asserted c
onnectivities');
#47713=(
GEOMETRIC_REPRESENTATION_CONTEXT(3)
GLOBAL_UNCERTAINTY_ASSIGNED_CONTEXT((#47699))
GLOBAL_UNIT_ASSIGNED_CONTEXT((#47718,#47720,#47721))
REPRESENTATION_CONTEXT('','3D')
);
#47717=(
GEOMETRIC_REPRESENTATION_CONTEXT(3)
GLOBAL_UNCERTAINTY_ASSIGNED_CONTEXT((#47703))
GLOBAL_UNIT_ASSIGNED_CONTEXT((#47718,#47720,#47721))
REPRESENTATION_CONTEXT('','3D')
);
#47718=(
LENGTH_UNIT()
NAMED_UNIT(*)
SI_UNIT(.MILLI.,.METRE.)
);
#47720=(
NAMED_UNIT(*)
PLANE_ANGLE_UNIT()
SI_UNIT($,.RADIAN.)
);
#47721=(
NAMED_UNIT(*)
SI_UNIT($,.STERADIAN.)
SOLID_ANGLE_UNIT()
);
#47731=SHAPE_DEFINITION_REPRESENTATION(#47744,#47769);
#47744=PRODUCT_DEFINITION_SHAPE('',$,#47783);
#47769=SHAPE_REPRESENTATION('',(#9812),#47713);
#47773=PRODUCT_DEFINITION_CONTEXT('part definition',#47814,'design');
#47783=PRODUCT_DEFINITION('small pin','Small Pin',#47796,#47773);
#47796=PRODUCT_DEFINITION_FORMATION('',$,#47825);
#47814=APPLICATION_CONTEXT(
'Core Data for Automotive Mechanical Design Process');
#47815=PRODUCT_CONTEXT('part definition',#47814,'mechanical');
#47825=PRODUCT('small pin','Small Pin',$,(#47815));
#47830=PRESENTATION_STYLE_ASSIGNMENT((#47832));
#47832=SURFACE_STYLE_USAGE(.BOTH.,#47834);
#47834=SURFACE_SIDE_STYLE('',(#47836));
#47836=SURFACE_STYLE_FILL_AREA(#47838);
#47838=FILL_AREA_STYLE('Opaque(202,209,238)',(#47840));
#47840=FILL_AREA_STYLE_COLOUR('Opaque(202,209,238)',#47842);
#47842=COLOUR_RGB('Opaque(202,209,238)', 0.66274510, 0.83137255, 0.94901961);
ENDSEC;
END-ISO-10303-21;
